ISO-10303-21;
HEADER;
/* Generated by software containing ST-Developer
 * from STEP Tools, Inc. (www.steptools.com) 
 */

FILE_DESCRIPTION(
/* description */ ('Bin tilter linkage'),
/* implementation_level */ '2;1');

FILE_NAME(
/* name */ 'Feed screw.step',
/* time_stamp */ '2026-10-28T03:26:24-07:00',
/* author */ (''),
/* organization */ (''),
/* preprocessor_version */ 'ST-DEVELOPER v20.2',
/* originating_system */ 'Autodesk Translation Framework v15.17.0.0',
/* authorisation */ '');

FILE_SCHEMA (('AUTOMOTIVE_DESIGN { 1 0 10303 214 3 1 1 }'));
ENDSEC;

DATA;
#10=MECHANICAL_DESIGN_GEOMETRIC_PRESENTATION_REPRESENTATION('',(#971),#23728);
#751=SHAPE_REPRESENTATION_RELATIONSHIP('SRR','None',#24223,#857);
#857=ADVANCED_BREP_SHAPE_REPRESENTATION('',(#1082),#23723);
#971=STYLED_ITEM('',(#24772),#1082);
#1082=MANIFOLD_SOLID_BREP('Body1',#12504);
#1880=PLANE('',#15427);
#1881=PLANE('',#15428);
#2649=FACE_OUTER_BOUND('',#3825,.T.);
#2650=FACE_OUTER_BOUND('',#3826,.T.);
#2651=FACE_OUTER_BOUND('',#3827,.T.);
#3825=EDGE_LOOP('',(#11219,#11220,#11221,#11222));
#3826=EDGE_LOOP('',(#11223));
#3827=EDGE_LOOP('',(#11224));
#4516=LINE('',#23425,#5191);
#5191=VECTOR('',#19641,0.6);
#5941=CIRCLE('',#15425,0.6);
#5942=CIRCLE('',#15426,0.6);
#6910=VERTEX_POINT('',#23422);
#6911=VERTEX_POINT('',#23424);
#8349=EDGE_CURVE('',#6910,#6910,#5941,.T.);
#8350=EDGE_CURVE('',#6910,#6911,#4516,.T.);
#8351=EDGE_CURVE('',#6911,#6911,#5942,.T.);
#11219=ORIENTED_EDGE('',*,*,#8349,.F.);
#11220=ORIENTED_EDGE('',*,*,#8350,.T.);
#11221=ORIENTED_EDGE('',*,*,#8351,.T.);
#11222=ORIENTED_EDGE('',*,*,#8350,.F.);
#11223=ORIENTED_EDGE('',*,*,#8349,.T.);
#11224=ORIENTED_EDGE('',*,*,#8351,.F.);
#11607=CYLINDRICAL_SURFACE('',#15424,0.6);
#12374=ADVANCED_FACE('',(#2649),#11607,.T.);
#12375=ADVANCED_FACE('',(#2650),#1880,.T.);
#12376=ADVANCED_FACE('',(#2651),#1881,.F.);
#12504=CLOSED_SHELL('',(#12374,#12375,#12376));
#15423=AXIS2_PLACEMENT_3D('',#23420,#19635,#19636);
#15424=AXIS2_PLACEMENT_3D('',#23421,#19637,#19638);
#15425=AXIS2_PLACEMENT_3D('',#23423,#19639,#19640);
#15426=AXIS2_PLACEMENT_3D('',#23426,#19642,#19643);
#15427=AXIS2_PLACEMENT_3D('',#23427,#19644,#19645);
#15428=AXIS2_PLACEMENT_3D('',#23428,#19646,#19647);
#19635=DIRECTION('axis',(0.,0.,1.));
#19636=DIRECTION('refdir',(1.,0.,0.));
#19637=DIRECTION('center_axis',(1.,0.,0.));
#19638=DIRECTION('ref_axis',(0.,0.,-1.));
#19639=DIRECTION('center_axis',(1.,0.,0.));
#19640=DIRECTION('ref_axis',(0.,0.,-1.));
#19641=DIRECTION('',(-1.,0.,0.));
#19642=DIRECTION('center_axis',(1.,0.,0.));
#19643=DIRECTION('ref_axis',(0.,0.,-1.));
#19644=DIRECTION('center_axis',(1.,0.,0.));
#19645=DIRECTION('ref_axis',(0.,0.,-1.));
#19646=DIRECTION('center_axis',(1.,0.,0.));
#19647=DIRECTION('ref_axis',(0.,0.,-1.));
#23420=CARTESIAN_POINT('',(0.,0.,0.));
#23421=CARTESIAN_POINT('Origin',(-12.5,-4.5,8.));
#23422=CARTESIAN_POINT('',(2.,-4.5,8.6));
#23423=CARTESIAN_POINT('Origin',(2.,-4.5,8.));
#23424=CARTESIAN_POINT('',(-12.5,-4.5,8.6));
#23425=CARTESIAN_POINT('',(-12.5,-4.5,8.6));
#23426=CARTESIAN_POINT('Origin',(-12.5,-4.5,8.));
#23427=CARTESIAN_POINT('Origin',(2.,-4.5,8.));
#23428=CARTESIAN_POINT('Origin',(-12.5,-4.5,8.));
#23606=UNCERTAINTY_MEASURE_WITH_UNIT(LENGTH_MEASURE(0.001),#23729,
'DISTANCE_ACCURACY_VALUE',
'Maximum model space distance between geometric entities at asserted c
onnectivities');
#23611=UNCERTAINTY_MEASURE_WITH_UNIT(LENGTH_MEASURE(0.001),#23729,
'DISTANCE_ACCURACY_VALUE',
'Maximum model space distance between geometric entities at asserted c
onnectivities');
#23723=(
GEOMETRIC_REPRESENTATION_CONTEXT(3)
GLOBAL_UNCERTAINTY_ASSIGNED_CONTEXT((#23606))
GLOBAL_UNIT_ASSIGNED_CONTEXT((#23729,#23731,#23732))
REPRESENTATION_CONTEXT('','3D')
);
#23728=(
GEOMETRIC_REPRESENTATION_CONTEXT(3)
GLOBAL_UNCERTAINTY_ASSIGNED_CONTEXT((#23611))
GLOBAL_UNIT_ASSIGNED_CONTEXT((#23729,#23731,#23732))
REPRESENTATION_CONTEXT('','3D')
);
#23729=(
LENGTH_UNIT()
NAMED_UNIT(*)
SI_UNIT(.CENTI.,.METRE.)
);
#23731=(
NAMED_UNIT(*)
PLANE_ANGLE_UNIT()
SI_UNIT($,.RADIAN.)
);
#23732=(
NAMED_UNIT(*)
SI_UNIT($,.STERADIAN.)
SOLID_ANGLE_UNIT()
);
#23844=SHAPE_DEFINITION_REPRESENTATION(#24095,#24223);
#24095=PRODUCT_DEFINITION_SHAPE('',$,#24340);
#24223=SHAPE_REPRESENTATION('',(#15423),#23723);
#24228=PRODUCT_DEFINITION_CONTEXT('part definition',#24578,'design');
#24340=PRODUCT_DEFINITION('Feed screw','Feed screw',#24456,#24228);
#24456=PRODUCT_DEFINITION_FORMATION('',$,#24691);
#24578=APPLICATION_CONTEXT(
'Core Data for Automotive Mechanical Design Process');
#24579=PRODUCT_CONTEXT('part definition',#24578,'mechanical');
#24691=PRODUCT('Feed screw','Feed screw','Feed screw',(#24579));
#24766=COLOUR_RGB('Black',0.12,0.14,0.17);
#24767=FILL_AREA_STYLE_COLOUR('',#24766);
#24768=FILL_AREA_STYLE('',(#24767));
#24769=SURFACE_STYLE_FILL_AREA(#24768);
#24770=SURFACE_SIDE_STYLE('',(#24769));
#24771=SURFACE_STYLE_USAGE(.BOTH.,#24770);
#24772=PRESENTATION_STYLE_ASSIGNMENT((#24771));
ENDSEC;
END-ISO-10303-21;
